ISO-10303-21;
HEADER;
FILE_DESCRIPTION (('STEP AP214'),
    '1' );
FILE_NAME ('rubber for air flow regulation.step',
    '2026-10-05T20:10:51',
    ( '' ),
    ( '' ),
    'SwSTEP 2.0',
    'SolidWorks 2020',
    '' );
FILE_SCHEMA (( 'AUTOMOTIVE_DESIGN' ));
ENDSEC;

DATA;
#103=CARTESIAN_POINT ( 'NONE',  ( 1.255262969126037044E-15, 0.4999999999999998890, -10.24999999999999822 ) ) ;
#566=ORIENTED_EDGE ( 'NONE', *, *, #158591, .T. ) ;
#939=AXIS2_PLACEMENT_3D ( 'NONE', #116182, #182168, #33798 ) ;
#1071=VERTEX_POINT ( 'NONE', #103 ) ;
#1194=ORIENTED_EDGE ( 'NONE', *, *, #33879, .F. ) ;
#2270=AXIS2_PLACEMENT_3D ( 'NONE', #97155, #179457, #182625 ) ;
#4327=AXIS2_PLACEMENT_3D ( 'NONE', #23364, #22282, #38574 ) ;
#4492=CIRCLE ( 'NONE', #21638, 10.24999999999999822 ) ;
#5670=ADVANCED_FACE ( 'NONE', ( #74704 ), #73631, .T. ) ;
#6407=VERTEX_POINT ( 'NONE', #11934 ) ;
#6708=DIRECTION ( 'NONE',  ( 0.000000000000000000, 0.000000000000000000, 1.000000000000000000 ) ) ;
#8780=DIRECTION ( 'NONE',  ( -0.000000000000000000, -1.000000000000000000, -0.000000000000000000 ) ) ;
#8805=CIRCLE ( 'NONE', #154154, 0.2000000000000005107 ) ;
#8990=ORIENTED_EDGE ( 'NONE', *, *, #65446, .T. ) ;
#9793=DIRECTION ( 'NONE',  ( -0.000000000000000000, -1.000000000000000000, -0.000000000000000000 ) ) ;
#11709=ORIENTED_EDGE ( 'NONE', *, *, #108573, .T. ) ;
#11740=EDGE_CURVE ( 'NONE', #76194, #55540, #76041, .T. ) ;
#11934=CARTESIAN_POINT ( 'NONE',  ( 10.12374542407608935, 0.2401923788623722134, -4.551898349974264235 ) ) ;
#12110=SHAPE_REPRESENTATION_RELATIONSHIP ( 'NONE' , 'NONE' ,  #40301, #171430 ) ;
#13178=PRESENTATION_STYLE_ASSIGNMENT (( #194059 ) ) ;
#13338=ORIENTED_EDGE ( 'NONE', *, *, #108573, .F. ) ;
#14877=( NAMED_UNIT ( * ) PLANE_ANGLE_UNIT ( ) SI_UNIT ( $, .RADIAN. ) );
#15694=DIRECTION ( 'NONE',  ( 0.000000000000000000, 0.000000000000000000, 1.000000000000000000 ) ) ;
#15728=AXIS2_PLACEMENT_3D ( 'NONE', #192854, #79117, #145232 ) ;
#15957=FILL_AREA_STYLE_COLOUR ( '', #202953 ) ;
#16373=UNCERTAINTY_MEASURE_WITH_UNIT (LENGTH_MEASURE( 1.000000000000000082E-05 ), #147075, 'distance_accuracy_value', 'NONE');
#17173=DIRECTION ( 'NONE',  ( 0.000000000000000000, 0.000000000000000000, 1.000000000000000000 ) ) ;
#17179=DIRECTION ( 'NONE',  ( -0.000000000000000000, 1.000000000000000000, -0.000000000000000000 ) ) ;
#17592=AXIS2_PLACEMENT_3D ( 'NONE', #58066, #123172, #15694 ) ;
#17797=AXIS2_PLACEMENT_3D ( 'NONE', #148285, #17179, #33449 ) ;
#17933=PRODUCT_CONTEXT ( 'NONE', #38036, 'mechanical' ) ;
#18025=DIRECTION ( 'NONE',  ( -1.000000000000000000, 0.000000000000000000, 0.000000000000000000 ) ) ;
#21638=AXIS2_PLACEMENT_3D ( 'NONE', #76796, #158079, #105067 ) ;
#21809=CIRCLE ( 'NONE', #63285, 11.09999999999999964 ) ;
#22282=DIRECTION ( 'NONE',  ( -0.000000000000000000, -1.000000000000000000, -0.000000000000000000 ) ) ;
#22875=( LENGTH_UNIT ( ) NAMED_UNIT ( * ) SI_UNIT ( .MILLI., .METRE. ) );
#23364=CARTESIAN_POINT ( 'NONE',  ( 3.469446951953614189E-15, 0.7598076211376182387, 6.938893903907228378E-15 ) ) ;
#23410=( LENGTH_UNIT ( ) NAMED_UNIT ( * ) SI_UNIT ( .MILLI., .METRE. ) );
#23435=VERTEX_POINT ( 'NONE', #206105 ) ;
#23580=CARTESIAN_POINT ( 'NONE',  ( 1.316495309083404618E-15, 0.5000000000000000000, -10.75000000000000000 ) ) ;
#23771=ORIENTED_EDGE ( 'NONE', *, *, #110855, .F. ) ;
#24458=COLOUR_RGB ( '', 0.09019608, 0.27058824, 0.51372549) ;
#25556=FILL_AREA_STYLE_COLOUR ( '', #152593 ) ;
#26565=PRODUCT_DEFINITION ( 'UNKNOWN', '', #183724, #212877 ) ;
#27235=CARTESIAN_POINT ( 'NONE',  ( 0.000000000000000000, 0.06698729810653621108, 0.000000000000000000 ) ) ;
#27292=SURFACE_SIDE_STYLE ('',( #175702 ) ) ;
#27303=ORIENTED_EDGE ( 'NONE', *, *, #89264, .F. ) ;
#29523=STYLED_ITEM ( 'NONE', ( #171283 ), #94887 ) ;
#29899=PRODUCT ( 'rubber for air flow regulation', 'rubber for air flow regulation', '', ( #17933 ) ) ;
#30854=CARTESIAN_POINT ( 'NONE',  ( 0.000000000000000000, 0.4999999999999998890, 10.24999999999999822 ) ) ;
#31557=EDGE_LOOP ( 'NONE', ( #142828, #98739, #11709, #186001, #62870, #89820 ) ) ;
#32052=CARTESIAN_POINT ( 'NONE',  ( 0.000000000000000000, 0.5000000000000000000, 0.000000000000000000 ) ) ;
#32123=AXIS2_PLACEMENT_3D ( 'NONE', #171223, #38037, #158195 ) ;
#32392=FACE_OUTER_BOUND ( 'NONE', #77688, .T. ) ;
#32693=ORIENTED_EDGE ( 'NONE', *, *, #148616, .T. ) ;
#33449=DIRECTION ( 'NONE',  ( 0.000000000000000000, 0.000000000000000000, 1.000000000000000000 ) ) ;
#33798=DIRECTION ( 'NONE',  ( 0.000000000000000000, 0.000000000000000000, 1.000000000000000000 ) ) ;
#33879=EDGE_CURVE ( 'NONE', #83886, #163739, #41012, .T. ) ;
#34464=UNCERTAINTY_MEASURE_WITH_UNIT (LENGTH_MEASURE( 1.000000000000000082E-05 ), #22875, 'distance_accuracy_value', 'NONE');
#34505=CARTESIAN_POINT ( 'NONE',  ( 1.734723475976807094E-15, 0.7598076211376200151, -10.89999999999920632 ) ) ;
#36292=EDGE_CURVE ( 'NONE', #173148, #76194, #113896, .T. ) ;
#37207=ORIENTED_EDGE ( 'NONE', *, *, #36292, .T. ) ;
#37586=EDGE_CURVE ( 'NONE', #179011, #168570, #161911, .T. ) ;
#37903=ORIENTED_EDGE ( 'NONE', *, *, #182978, .T. ) ;
#38036=APPLICATION_CONTEXT ( 'automotive_design' ) ;
#38037=DIRECTION ( 'NONE',  ( 0.000000000000000000, 1.000000000000000000, 0.000000000000000000 ) ) ;
#38574=DIRECTION ( 'NONE',  ( 0.000000000000000000, 0.000000000000000000, -1.000000000000000000 ) ) ;
#38854=CIRCLE ( 'NONE', #4327, 11.09999999999999964 ) ;
#39976=DIRECTION ( 'NONE',  ( -0.000000000000000000, -1.000000000000000000, -0.000000000000000000 ) ) ;
#40077=DIRECTION ( 'NONE',  ( 0.000000000000000000, 1.000000000000000000, 0.000000000000000000 ) ) ;
#40301=SHAPE_REPRESENTATION ( 'rubber for air flow regulation', ( #200407 ), #135205 ) ;
#40771=FACE_OUTER_BOUND ( 'NONE', #206018, .T. ) ;
#41012=CIRCLE ( 'NONE', #186311, 11.09999999999999964 ) ;
#41580=AXIS2_PLACEMENT_3D ( 'NONE', #157578, #60056, #192173 ) ;
#41845=PRESENTATION_STYLE_ASSIGNMENT (( #190189 ) ) ;
#42149=DIRECTION ( 'NONE',  ( 0.000000000000000000, 0.000000000000000000, -1.000000000000000000 ) ) ;
#42227=SURFACE_STYLE_USAGE ( .BOTH. , #109416 ) ;
#43205=DIRECTION ( 'NONE',  ( 1.000000000000000000, 0.000000000000000000, -1.224646799147353207E-16 ) ) ;
#43580=( NAMED_UNIT ( * ) SI_UNIT ( $, .STERADIAN. ) SOLID_ANGLE_UNIT ( ) );
#46638=FACE_OUTER_BOUND ( 'NONE', #108779, .T. ) ;
#46934=ORIENTED_EDGE ( 'NONE', *, *, #182978, .F. ) ;
#47297=CARTESIAN_POINT ( 'NONE',  ( -10.12374542407608402, 0.7598076211376182387, 4.551898349974277558 ) ) ;
#47315=( GEOMETRIC_REPRESENTATION_CONTEXT ( 3 ) GLOBAL_UNCERTAINTY_ASSIGNED_CONTEXT ( ( #16373 ) ) GLOBAL_UNIT_ASSIGNED_CONTEXT ( ( #147075, #100432, #84182 ) ) REPRESENTATION_CONTEXT ( 'NONE', 'WORKASPACE' ) );
#47430=( LENGTH_UNIT ( ) NAMED_UNIT ( * ) SI_UNIT ( .MILLI., .METRE. ) );
#48216=CARTESIAN_POINT ( 'NONE',  ( 1.734723475976807094E-15, 0.2401923788623739342, 10.89999999999920810 ) ) ;
#49626=VERTEX_POINT ( 'NONE', #174574 ) ;
#50616=CARTESIAN_POINT ( 'NONE',  ( 1.734723475976807094E-15, 0.7598076211376200151, 3.469446951953614189E-15 ) ) ;
#52562=CARTESIAN_POINT ( 'NONE',  ( 3.469446951953614189E-15, 0.2401923788623722134, 6.938893903907228378E-15 ) ) ;
#52752=ORIENTED_EDGE ( 'NONE', *, *, #89264, .T. ) ;
#53219=DIRECTION ( 'NONE',  ( 0.000000000000000000, 0.000000000000000000, -1.000000000000000000 ) ) ;
#53727=EDGE_CURVE ( 'NONE', #6407, #55540, #191136, .T. ) ;
#53967=DIRECTION ( 'NONE',  ( 1.000000000000000000, 0.000000000000000000, 1.224646799147353207E-16 ) ) ;
#54271=DIRECTION ( 'NONE',  ( 1.224646799147353454E-16, 0.000000000000000000, -1.000000000000000000 ) ) ;
#55261=FILL_AREA_STYLE_COLOUR ( '', #212363 ) ;
#55540=VERTEX_POINT ( 'NONE', #153367 ) ;
#56475=CARTESIAN_POINT ( 'NONE',  ( 1.734723475976807094E-15, 0.7598076211376200151, 3.469446951953614189E-15 ) ) ;
#56949=CLOSED_SHELL ( 'NONE', ( #178480, #60355, #94887, #170365, #5670, #77216, #94031, #197373, #115976, #99975 ) ) ;
#57046=CARTESIAN_POINT ( 'NONE',  ( 3.469446951953614189E-15, 0.7598076211376182387, 6.938893903907228378E-15 ) ) ;
#57384=DIRECTION ( 'NONE',  ( 0.9120491373041519356, 0.000000000000000000, -0.4100809324301145642 ) ) ;
#57984=VERTEX_POINT ( 'NONE', #204669 ) ;
#58066=CARTESIAN_POINT ( 'NONE',  ( 1.734723475976807094E-15, 0.2401923788623739342, 3.469446951953614189E-15 ) ) ;
#58553=CARTESIAN_POINT ( 'NONE',  ( 3.469446951953614189E-15, 0.7598076211376182387, 6.938893903907228378E-15 ) ) ;
#59668=CIRCLE ( 'NONE', #128852, 0.5000000000000004441 ) ;
#60056=DIRECTION ( 'NONE',  ( 1.000000000000000000, -0.000000000000000000, 1.224646799147353207E-16 ) ) ;
#60237=AXIS2_PLACEMENT_3D ( 'NONE', #121408, #107272, #137590 ) ;
#60355=ADVANCED_FACE ( 'NONE', ( #32392 ), #111295, .T. ) ;
#60703=AXIS2_PLACEMENT_3D ( 'NONE', #171912, #204374, #123260 ) ;
#61506=ORIENTED_EDGE ( 'NONE', *, *, #53727, .F. ) ;
#62595=TOROIDAL_SURFACE ( 'NONE', #17592, 10.89999999999920632, 0.2000000000000000111 ) ;
#62870=ORIENTED_EDGE ( 'NONE', *, *, #90474, .T. ) ;
#63285=AXIS2_PLACEMENT_3D ( 'NONE', #52562, #153261, #186820 ) ;
#63399=EDGE_CURVE ( 'NONE', #57984, #83886, #38854, .T. ) ;
#63608=DIRECTION ( 'NONE',  ( 0.000000000000000000, 0.000000000000000000, 1.000000000000000000 ) ) ;
#63657=( NAMED_UNIT ( * ) SI_UNIT ( $, .STERADIAN. ) SOLID_ANGLE_UNIT ( ) );
#64464=VERTEX_POINT ( 'NONE', #132171 ) ;
#64551=DIRECTION ( 'NONE',  ( 0.000000000000000000, 0.000000000000000000, 1.000000000000000000 ) ) ;
#64712=FILL_AREA_STYLE ('',( #79894 ) ) ;
#65446=EDGE_CURVE ( 'NONE', #103667, #1071, #4492, .T. ) ;
#65459=EDGE_CURVE ( 'NONE', #163739, #49626, #191276, .T. ) ;
#65733=ORIENTED_EDGE ( 'NONE', *, *, #114579, .T. ) ;
#65763=FACE_OUTER_BOUND ( 'NONE', #203462, .T. ) ;
#66088=EDGE_CURVE ( 'NONE', #64464, #6407, #21809, .T. ) ;
#66826=DIRECTION ( 'NONE',  ( 0.000000000000000000, 0.000000000000000000, -1.000000000000000000 ) ) ;
#67774=CIRCLE ( 'NONE', #178387, 0.5000000000000004441 ) ;
#67965=AXIS2_PLACEMENT_3D ( 'NONE', #23580, #53967, #204448 ) ;
#71068=COLOUR_RGB ( '', 0.72549020, 0.75294118, 0.79215686) ;
#71534=TOROIDAL_SURFACE ( 'NONE', #199556, 10.89999999999920988, 0.2000000000000000111 ) ;
#72528=DIRECTION ( 'NONE',  ( 0.000000000000000000, 0.000000000000000000, -1.000000000000000000 ) ) ;
#72958=MECHANICAL_DESIGN_GEOMETRIC_PRESENTATION_REPRESENTATION('',(#156011),#149036);
#73631=CYLINDRICAL_SURFACE ( 'NONE', #126322, 11.10000000000000320 ) ;
#73636=FACE_OUTER_BOUND ( 'NONE', #146579, .T. ) ;
#73734=DIRECTION ( 'NONE',  ( 0.000000000000000000, 0.000000000000000000, -1.000000000000000000 ) ) ;
#74341=ORIENTED_EDGE ( 'NONE', *, *, #193470, .F. ) ;
#74515=TOROIDAL_SURFACE ( 'NONE', #195576, 10.89999999999920988, 0.2000000000000000111 ) ;
#74704=FACE_OUTER_BOUND ( 'NONE', #31557, .T. ) ;
#75391=FILL_AREA_STYLE ('',( #25556 ) ) ;
#76041=CIRCLE ( 'NONE', #41580, 0.2000000000000005107 ) ;
#76111=ORIENTED_EDGE ( 'NONE', *, *, #193470, .T. ) ;
#76194=VERTEX_POINT ( 'NONE', #210619 ) ;
#76269=MECHANICAL_DESIGN_GEOMETRIC_PRESENTATION_REPRESENTATION('',(#180038),#110972);
#76781=AXIS2_PLACEMENT_3D ( 'NONE', #209008, #126807, #139799 ) ;
#76796=CARTESIAN_POINT ( 'NONE',  ( 0.000000000000000000, 0.4999999999999998890, 0.000000000000000000 ) ) ;
#76881=CARTESIAN_POINT ( 'NONE',  ( -10.12374542407608757, -16.99999999999999645, 4.551898349974279334 ) ) ;
#77216=ADVANCED_FACE ( 'NONE', ( #175489 ), #163387, .T. ) ;
#77688=EDGE_LOOP ( 'NONE', ( #206357, #8990, #141053, #65733 ) ) ;
#78362=CIRCLE ( 'NONE', #130404, 11.09999999999999964 ) ;
#78735=DIRECTION ( 'NONE',  ( 0.000000000000000000, 1.000000000000000000, 0.000000000000000000 ) ) ;
#78839=AXIS2_PLACEMENT_3D ( 'NONE', #140736, #206748, #42149 ) ;
#79117=DIRECTION ( 'NONE',  ( -0.000000000000000000, 1.000000000000000000, -0.000000000000000000 ) ) ;
#79255=( LENGTH_UNIT ( ) NAMED_UNIT ( * ) SI_UNIT ( .MILLI., .METRE. ) );
#79894=FILL_AREA_STYLE_COLOUR ( '', #160953 ) ;
#81294=ORIENTED_EDGE ( 'NONE', *, *, #147718, .F. ) ;
#82142=UNCERTAINTY_MEASURE_WITH_UNIT (LENGTH_MEASURE( 1.000000000000000082E-05 ), #47430, 'distance_accuracy_value', 'NONE');
#83886=VERTEX_POINT ( 'NONE', #161803 ) ;
#84182=( NAMED_UNIT ( * ) SI_UNIT ( $, .STERADIAN. ) SOLID_ANGLE_UNIT ( ) );
#84887=DIRECTION ( 'NONE',  ( 0.000000000000000000, 1.000000000000000000, 0.000000000000000000 ) ) ;
#85149=UNCERTAINTY_MEASURE_WITH_UNIT (LENGTH_MEASURE( 1.000000000000000082E-05 ), #23410, 'distance_accuracy_value', 'NONE');
#85771=FACE_OUTER_BOUND ( 'NONE', #186979, .T. ) ;
#86537=EDGE_CURVE ( 'NONE', #179011, #49626, #191853, .T. ) ;
#87643=MANIFOLD_SOLID_BREP ( 'Fillet1', #56949 ) ;
#88589=ORIENTED_EDGE ( 'NONE', *, *, #66088, .T. ) ;
#89264=EDGE_CURVE ( 'NONE', #168570, #83886, #8805, .T. ) ;
#89521=( NAMED_UNIT ( * ) PLANE_ANGLE_UNIT ( ) SI_UNIT ( $, .RADIAN. ) );
#89820=ORIENTED_EDGE ( 'NONE', *, *, #124072, .F. ) ;
#89908=CARTESIAN_POINT ( 'NONE',  ( 3.469446951953614189E-15, -16.99999999999999645, 6.938893903907228378E-15 ) ) ;
#90474=EDGE_CURVE ( 'NONE', #49626, #57984, #195276, .T. ) ;
#90969=AXIS2_PLACEMENT_3D ( 'NONE', #122459, #107245, #72528 ) ;
#92343=( NAMED_UNIT ( * ) PLANE_ANGLE_UNIT ( ) SI_UNIT ( $, .RADIAN. ) );
#94031=ADVANCED_FACE ( 'NONE', ( #46638 ), #157543, .T. ) ;
#94465=FILL_AREA_STYLE_COLOUR ( '', #24458 ) ;
#94887=ADVANCED_FACE ( 'NONE', ( #85771 ), #74515, .T. ) ;
#95216=CARTESIAN_POINT ( 'NONE',  ( 0.000000000000000000, 0.000000000000000000, 0.000000000000000000 ) ) ;
#95260=MECHANICAL_DESIGN_GEOMETRIC_PRESENTATION_REPRESENTATION('',(#119428),#123010);
#95716=CIRCLE ( 'NONE', #2270, 0.5000000000000004441 ) ;
#95849=ORIENTED_EDGE ( 'NONE', *, *, #90474, .F. ) ;
#97155=CARTESIAN_POINT ( 'NONE',  ( 0.000000000000000000, 0.5000000000000000000, 10.75000000000000000 ) ) ;
#98474=DIRECTION ( 'NONE',  ( 0.000000000000000000, 1.000000000000000000, 0.000000000000000000 ) ) ;
#98739=ORIENTED_EDGE ( 'NONE', *, *, #110855, .T. ) ;
#99975=ADVANCED_FACE ( 'NONE', ( #65763 ), #71534, .T. ) ;
#100432=( NAMED_UNIT ( * ) PLANE_ANGLE_UNIT ( ) SI_UNIT ( $, .RADIAN. ) );
#101336=SHAPE_DEFINITION_REPRESENTATION ( #109439, #40301 ) ;
#103667=VERTEX_POINT ( 'NONE', #30854 ) ;
#104995=ORIENTED_EDGE ( 'NONE', *, *, #148616, .F. ) ;
#105067=DIRECTION ( 'NONE',  ( 0.000000000000000000, 0.000000000000000000, 1.000000000000000000 ) ) ;
#105243=SURFACE_STYLE_FILL_AREA ( #187529 ) ;
#107245=DIRECTION ( 'NONE',  ( -0.000000000000000000, -1.000000000000000000, -0.000000000000000000 ) ) ;
#107272=DIRECTION ( 'NONE',  ( 0.000000000000000000, 1.000000000000000000, 0.000000000000000000 ) ) ;
#108573=EDGE_CURVE ( 'NONE', #23435, #163739, #177603, .T. ) ;
#108779=EDGE_LOOP ( 'NONE', ( #201227, #74341, #109012, #32693 ) ) ;
#109012=ORIENTED_EDGE ( 'NONE', *, *, #37586, .T. ) ;
#109416=SURFACE_SIDE_STYLE ('',( #125670 ) ) ;
#109439=PRODUCT_DEFINITION_SHAPE ( 'NONE', 'NONE',  #26565 ) ;
#110207=APPLICATION_CONTEXT ( 'automotive_design' ) ;
#110399=EDGE_LOOP ( 'NONE', ( #13338, #121596, #88589, #130605, #148939, #153979 ) ) ;
#110855=EDGE_CURVE ( 'NONE', #55540, #23435, #111663, .T. ) ;
#110972=( GEOMETRIC_REPRESENTATION_CONTEXT ( 3 ) GLOBAL_UNCERTAINTY_ASSIGNED_CONTEXT ( ( #134864 ) ) GLOBAL_UNIT_ASSIGNED_CONTEXT ( ( #79255, #92343, #160506 ) ) REPRESENTATION_CONTEXT ( 'NONE', 'WORKASPACE' ) );
#111295=TOROIDAL_SURFACE ( 'NONE', #17797, 10.75000000000000000, 0.5000000000000007772 ) ;
#111663=CIRCLE ( 'NONE', #32123, 11.09999999999999964 ) ;
#111974=AXIS2_PLACEMENT_3D ( 'NONE', #27235, #155126, #6708 ) ;
#112126=MECHANICAL_DESIGN_GEOMETRIC_PRESENTATION_REPRESENTATION('',(#119060),#164014);
#113896=CIRCLE ( 'NONE', #196832, 10.99999999999718980 ) ;
#114579=EDGE_CURVE ( 'NONE', #76194, #173148, #205256, .T. ) ;
#114621=SURFACE_STYLE_FILL_AREA ( #167572 ) ;
#114626=ORIENTED_EDGE ( 'NONE', *, *, #66088, .F. ) ;
#115976=ADVANCED_FACE ( 'NONE', ( #73636 ), #170942, .T. ) ;
#116182=CARTESIAN_POINT ( 'NONE',  ( 3.469446951953614189E-15, 0.2401923788623722134, 6.938893903907228378E-15 ) ) ;
#116741=DIRECTION ( 'NONE',  ( -0.000000000000000000, -1.000000000000000000, -0.000000000000000000 ) ) ;
#119060=STYLED_ITEM ( 'NONE', ( #154898 ), #115976 ) ;
#119306=ORIENTED_EDGE ( 'NONE', *, *, #65446, .F. ) ;
#119403=SURFACE_STYLE_USAGE ( .BOTH. , #152904 ) ;
#119428=STYLED_ITEM ( 'NONE', ( #130855 ), #87643 ) ;
#121408=CARTESIAN_POINT ( 'NONE',  ( 1.734723475976807094E-15, 0.2401923788623739342, 3.469446951953614189E-15 ) ) ;
#121596=ORIENTED_EDGE ( 'NONE', *, *, #148262, .T. ) ;
#121679=CARTESIAN_POINT ( 'NONE',  ( 0.000000000000000000, 0.06698729810653621108, 10.99999999999751665 ) ) ;
#122459=CARTESIAN_POINT ( 'NONE',  ( 3.469446951953614189E-15, 0.7598076211376182387, 6.938893903907228378E-15 ) ) ;
#123010=( GEOMETRIC_REPRESENTATION_CONTEXT ( 3 ) GLOBAL_UNCERTAINTY_ASSIGNED_CONTEXT ( ( #82142 ) ) GLOBAL_UNIT_ASSIGNED_CONTEXT ( ( #47430, #14877, #63657 ) ) REPRESENTATION_CONTEXT ( 'NONE', 'WORKASPACE' ) );
#123172=DIRECTION ( 'NONE',  ( 0.000000000000000000, 1.000000000000000000, 0.000000000000000000 ) ) ;
#123260=DIRECTION ( 'NONE',  ( 0.000000000000000000, 0.000000000000000000, 1.000000000000000000 ) ) ;
#123553=( LENGTH_UNIT ( ) NAMED_UNIT ( * ) SI_UNIT ( .MILLI., .METRE. ) );
#124072=EDGE_CURVE ( 'NONE', #6407, #57984, #199687, .T. ) ;
#124147=ORIENTED_EDGE ( 'NONE', *, *, #158591, .F. ) ;
#124230=SURFACE_SIDE_STYLE ('',( #188051 ) ) ;
#124612=ORIENTED_EDGE ( 'NONE', *, *, #11740, .T. ) ;
#125028=ORIENTED_EDGE ( 'NONE', *, *, #86537, .F. ) ;
#125670=SURFACE_STYLE_FILL_AREA ( #205759 ) ;
#126322=AXIS2_PLACEMENT_3D ( 'NONE', #89908, #40077, #57384 ) ;
#126518=CARTESIAN_POINT ( 'NONE',  ( 3.469446951953614189E-15, 0.2401923788623722134, 6.938893903907228378E-15 ) ) ;
#126676=ORIENTED_EDGE ( 'NONE', *, *, #148262, .F. ) ;
#126807=DIRECTION ( 'NONE',  ( -0.000000000000000000, 1.000000000000000000, -0.000000000000000000 ) ) ;
#128852=AXIS2_PLACEMENT_3D ( 'NONE', #166434, #18025, #63608 ) ;
#130404=AXIS2_PLACEMENT_3D ( 'NONE', #126518, #78735, #176261 ) ;
#130605=ORIENTED_EDGE ( 'NONE', *, *, #124072, .T. ) ;
#130855=PRESENTATION_STYLE_ASSIGNMENT (( #177415 ) ) ;
#131258=ORIENTED_EDGE ( 'NONE', *, *, #65459, .F. ) ;
#131518=ORIENTED_EDGE ( 'NONE', *, *, #114579, .F. ) ;
#132002=DIRECTION ( 'NONE',  ( 0.000000000000000000, 0.000000000000000000, 1.000000000000000000 ) ) ;
#132171=CARTESIAN_POINT ( 'NONE',  ( 1.734723475976807094E-15, 0.2401923788623722134, 11.09999999999960885 ) ) ;
#132969=SURFACE_STYLE_USAGE ( .BOTH. , #179562 ) ;
#133496=( NAMED_UNIT ( * ) PLANE_ANGLE_UNIT ( ) SI_UNIT ( $, .RADIAN. ) );
#134358=FACE_OUTER_BOUND ( 'NONE', #110399, .T. ) ;
#134864=UNCERTAINTY_MEASURE_WITH_UNIT (LENGTH_MEASURE( 1.000000000000000082E-05 ), #79255, 'distance_accuracy_value', 'NONE');
#135205=( GEOMETRIC_REPRESENTATION_CONTEXT ( 3 ) GLOBAL_UNCERTAINTY_ASSIGNED_CONTEXT ( ( #150032 ) ) GLOBAL_UNIT_ASSIGNED_CONTEXT ( ( #177834, #195145, #43580 ) ) REPRESENTATION_CONTEXT ( 'NONE', 'WORKASPACE' ) );
#135743=CARTESIAN_POINT ( 'NONE',  ( 1.347111479061785482E-15, 0.9330127018934565308, -10.99999999999752553 ) ) ;
#137297=CIRCLE ( 'NONE', #67965, 0.5000000000000004441 ) ;
#137590=DIRECTION ( 'NONE',  ( 0.000000000000000000, 0.000000000000000000, 1.000000000000000000 ) ) ;
#139376=DIRECTION ( 'NONE',  ( -0.000000000000000000, -1.000000000000000000, -0.000000000000000000 ) ) ;
#139735=( NAMED_UNIT ( * ) SI_UNIT ( $, .STERADIAN. ) SOLID_ANGLE_UNIT ( ) );
#139799=DIRECTION ( 'NONE',  ( 0.000000000000000000, 0.000000000000000000, 1.000000000000000000 ) ) ;
#139802=VECTOR ( 'NONE', #98474, 1000.000000000000000 ) ;
#140736=CARTESIAN_POINT ( 'NONE',  ( 0.000000000000000000, 0.9330127018934565308, 0.000000000000000000 ) ) ;
#140965=ORIENTED_EDGE ( 'NONE', *, *, #11740, .F. ) ;
#141053=ORIENTED_EDGE ( 'NONE', *, *, #147718, .T. ) ;
#141881=( NAMED_UNIT ( * ) PLANE_ANGLE_UNIT ( ) SI_UNIT ( $, .RADIAN. ) );
#142025=( NAMED_UNIT ( * ) SI_UNIT ( $, .STERADIAN. ) SOLID_ANGLE_UNIT ( ) );
#142828=ORIENTED_EDGE ( 'NONE', *, *, #53727, .T. ) ;
#145232=DIRECTION ( 'NONE',  ( 0.000000000000000000, 0.000000000000000000, 1.000000000000000000 ) ) ;
#146567=CIRCLE ( 'NONE', #208814, 10.99999999999719513 ) ;
#146579=EDGE_LOOP ( 'NONE', ( #140965, #184116, #566, #126676, #23771 ) ) ;
#146897=DIRECTION ( 'NONE',  ( -0.000000000000000000, 1.000000000000000000, -0.000000000000000000 ) ) ;
#147075=( LENGTH_UNIT ( ) NAMED_UNIT ( * ) SI_UNIT ( .MILLI., .METRE. ) );
#147718=EDGE_CURVE ( 'NONE', #1071, #76194, #137297, .T. ) ;
#148262=EDGE_CURVE ( 'NONE', #23435, #64464, #78362, .T. ) ;
#148285=CARTESIAN_POINT ( 'NONE',  ( 0.000000000000000000, 0.5000000000000000000, 0.000000000000000000 ) ) ;
#148568=ORIENTED_EDGE ( 'NONE', *, *, #63399, .F. ) ;
#148616=EDGE_CURVE ( 'NONE', #168570, #103667, #95716, .T. ) ;
#148939=ORIENTED_EDGE ( 'NONE', *, *, #63399, .T. ) ;
#149036=( GEOMETRIC_REPRESENTATION_CONTEXT ( 3 ) GLOBAL_UNCERTAINTY_ASSIGNED_CONTEXT ( ( #85149 ) ) GLOBAL_UNIT_ASSIGNED_CONTEXT ( ( #23410, #89521, #155574 ) ) REPRESENTATION_CONTEXT ( 'NONE', 'WORKASPACE' ) );
#149166=SURFACE_STYLE_FILL_AREA ( #64712 ) ;
#150032=UNCERTAINTY_MEASURE_WITH_UNIT (LENGTH_MEASURE( 1.000000000000000082E-05 ), #177834, 'distance_accuracy_value', 'NONE');
#150718=DIRECTION ( 'NONE',  ( 1.000000000000000000, 0.000000000000000000, 1.224646799147353207E-16 ) ) ;
#150974=CARTESIAN_POINT ( 'NONE',  ( 10.12374542407609290, -16.99999999999999645, -4.551898349974266011 ) ) ;
#151651=DIRECTION ( 'NONE',  ( 0.9120491373041519356, 0.000000000000000000, -0.4100809324301145642 ) ) ;
#151852=FILL_AREA_STYLE_COLOUR ( '', #71068 ) ;
#152017=AXIS2_PLACEMENT_3D ( 'NONE', #48216, #164084, #211736 ) ;
#152593=COLOUR_RGB ( '', 0.31764706, 0.68627451, 0.89019608) ;
#152904=SURFACE_SIDE_STYLE ('',( #105243 ) ) ;
#153261=DIRECTION ( 'NONE',  ( 0.000000000000000000, 1.000000000000000000, 0.000000000000000000 ) ) ;
#153367=CARTESIAN_POINT ( 'NONE',  ( 3.094081423030320538E-15, 0.2401923788623722134, -11.09999999999959819 ) ) ;
#153979=ORIENTED_EDGE ( 'NONE', *, *, #33879, .T. ) ;
#154154=AXIS2_PLACEMENT_3D ( 'NONE', #208851, #43205, #209917 ) ;
#154841=CYLINDRICAL_SURFACE ( 'NONE', #189177, 11.10000000000000320 ) ;
#154898=PRESENTATION_STYLE_ASSIGNMENT (( #42227 ) ) ;
#155126=DIRECTION ( 'NONE',  ( -0.000000000000000000, -1.000000000000000000, -0.000000000000000000 ) ) ;
#155574=( NAMED_UNIT ( * ) SI_UNIT ( $, .STERADIAN. ) SOLID_ANGLE_UNIT ( ) );
#156011=STYLED_ITEM ( 'NONE', ( #41845 ), #170365 ) ;
#157543=TOROIDAL_SURFACE ( 'NONE', #15728, 10.75000000000000000, 0.5000000000000007772 ) ;
#157578=CARTESIAN_POINT ( 'NONE',  ( 3.069588487047324915E-15, 0.2401923788623739342, -10.89999999999920277 ) ) ;
#158079=DIRECTION ( 'NONE',  ( -0.000000000000000000, 1.000000000000000000, -0.000000000000000000 ) ) ;
#158195=DIRECTION ( 'NONE',  ( 0.000000000000000000, 0.000000000000000000, 1.000000000000000000 ) ) ;
#158327=ORIENTED_EDGE ( 'NONE', *, *, #86537, .T. ) ;
#158591=EDGE_CURVE ( 'NONE', #173148, #64464, #165769, .T. ) ;
#160506=( NAMED_UNIT ( * ) SI_UNIT ( $, .STERADIAN. ) SOLID_ANGLE_UNIT ( ) );
#160953=COLOUR_RGB ( '', 0.09019608, 0.27058824, 0.51372549) ;
#161195=VECTOR ( 'NONE', #84887, 1000.000000000000000 ) ;
#161266=DIRECTION ( 'NONE',  ( 1.000000000000000000, 0.000000000000000000, 0.000000000000000000 ) ) ;
#161803=CARTESIAN_POINT ( 'NONE',  ( 3.094081423030320933E-15, 0.7598076211376182387, 11.09999999999961062 ) ) ;
#161911=CIRCLE ( 'NONE', #78839, 10.99999999999719513 ) ;
#163387=TOROIDAL_SURFACE ( 'NONE', #76781, 10.75000000000000000, 0.5000000000000007772 ) ;
#163739=VERTEX_POINT ( 'NONE', #47297 ) ;
#164014=( GEOMETRIC_REPRESENTATION_CONTEXT ( 3 ) GLOBAL_UNCERTAINTY_ASSIGNED_CONTEXT ( ( #211384 ) ) GLOBAL_UNIT_ASSIGNED_CONTEXT ( ( #123553, #141881, #139735 ) ) REPRESENTATION_CONTEXT ( 'NONE', 'WORKASPACE' ) );
#164084=DIRECTION ( 'NONE',  ( -1.000000000000000000, 0.000000000000000000, 0.000000000000000000 ) ) ;
#164942=STYLED_ITEM ( 'NONE', ( #196864 ), #99975 ) ;
#165579=DIRECTION ( 'NONE',  ( -1.000000000000000000, 0.000000000000000000, 0.000000000000000000 ) ) ;
#165769=CIRCLE ( 'NONE', #152017, 0.2000000000000005107 ) ;
#166434=CARTESIAN_POINT ( 'NONE',  ( 0.000000000000000000, 0.5000000000000000000, 10.75000000000000000 ) ) ;
#166829=CARTESIAN_POINT ( 'NONE',  ( 3.469446951953614189E-15, -16.99999999999999645, 6.938893903907228378E-15 ) ) ;
#167572=FILL_AREA_STYLE ('',( #15957 ) ) ;
#168106=ORIENTED_EDGE ( 'NONE', *, *, #191412, .T. ) ;
#168570=VERTEX_POINT ( 'NONE', #212325 ) ;
#170140=CARTESIAN_POINT ( 'NONE',  ( 1.316495309083404618E-15, 0.5000000000000000000, -10.75000000000000000 ) ) ;
#170365=ADVANCED_FACE ( 'NONE', ( #40771 ), #62595, .T. ) ;
#170942=TOROIDAL_SURFACE ( 'NONE', #60237, 10.89999999999920632, 0.2000000000000000111 ) ;
#171223=CARTESIAN_POINT ( 'NONE',  ( 3.469446951953614189E-15, 0.2401923788623722134, 6.938893903907228378E-15 ) ) ;
#171283=PRESENTATION_STYLE_ASSIGNMENT (( #119403 ) ) ;
#171430=ADVANCED_BREP_SHAPE_REPRESENTATION ( '', ( #87643, #200407 ), #135205 ) ;
#171912=CARTESIAN_POINT ( 'NONE',  ( 0.000000000000000000, 0.4999999999999998890, 0.000000000000000000 ) ) ;
#172107=DIRECTION ( 'NONE',  ( 0.000000000000000000, 0.000000000000000000, 1.000000000000000000 ) ) ;
#172364=DIRECTION ( 'NONE',  ( 0.000000000000000000, 0.000000000000000000, -1.000000000000000000 ) ) ;
#173148=VERTEX_POINT ( 'NONE', #121679 ) ;
#174574=CARTESIAN_POINT ( 'NONE',  ( 1.734723475976807094E-15, 0.7598076211376182387, -11.09999999999959996 ) ) ;
#174601=EDGE_CURVE ( 'NONE', #103667, #173148, #59668, .T. ) ;
#175082=DIRECTION ( 'NONE',  ( 0.000000000000000000, 0.000000000000000000, -1.000000000000000000 ) ) ;
#175201=EDGE_LOOP ( 'NONE', ( #81294, #168106, #199834, #37207 ) ) ;
#175489=FACE_OUTER_BOUND ( 'NONE', #194643, .T. ) ;
#175702=SURFACE_STYLE_FILL_AREA ( #210305 ) ;
#176261=DIRECTION ( 'NONE',  ( 0.000000000000000000, 0.000000000000000000, 1.000000000000000000 ) ) ;
#177415=SURFACE_STYLE_USAGE ( .BOTH. , #197903 ) ;
#177482=AXIS2_PLACEMENT_3D ( 'NONE', #32052, #146897, #64551 ) ;
#177603=LINE ( 'NONE', #76881, #139802 ) ;
#177834=( LENGTH_UNIT ( ) NAMED_UNIT ( * ) SI_UNIT ( .MILLI., .METRE. ) );
#178387=AXIS2_PLACEMENT_3D ( 'NONE', #170140, #150718, #54271 ) ;
#178480=ADVANCED_FACE ( 'NONE', ( #195629 ), #194783, .T. ) ;
#178718=MECHANICAL_DESIGN_GEOMETRIC_PRESENTATION_REPRESENTATION('',(#164942),#47315);
#179011=VERTEX_POINT ( 'NONE', #135743 ) ;
#179457=DIRECTION ( 'NONE',  ( -1.000000000000000000, 0.000000000000000000, 0.000000000000000000 ) ) ;
#179562=SURFACE_SIDE_STYLE ('',( #114621 ) ) ;
#180038=STYLED_ITEM ( 'NONE', ( #13178 ), #171430 ) ;
#182168=DIRECTION ( 'NONE',  ( 0.000000000000000000, 1.000000000000000000, 0.000000000000000000 ) ) ;
#182625=DIRECTION ( 'NONE',  ( 0.000000000000000000, 0.000000000000000000, 1.000000000000000000 ) ) ;
#182978=EDGE_CURVE ( 'NONE', #168570, #179011, #146567, .T. ) ;
#183724=PRODUCT_DEFINITION_FORMATION_WITH_SPECIFIED_SOURCE ( 'ANY', '', #29899, .NOT_KNOWN. ) ;
#184116=ORIENTED_EDGE ( 'NONE', *, *, #36292, .F. ) ;
#185363=AXIS2_PLACEMENT_3D ( 'NONE', #57046, #139376, #175082 ) ;
#186001=ORIENTED_EDGE ( 'NONE', *, *, #65459, .T. ) ;
#186311=AXIS2_PLACEMENT_3D ( 'NONE', #58553, #9793, #73734 ) ;
#186820=DIRECTION ( 'NONE',  ( 0.000000000000000000, 0.000000000000000000, 1.000000000000000000 ) ) ;
#186979=EDGE_LOOP ( 'NONE', ( #46934, #52752, #148568, #95849, #125028 ) ) ;
#187529=FILL_AREA_STYLE ('',( #151852 ) ) ;
#188051=SURFACE_STYLE_FILL_AREA ( #75391 ) ;
#188337=CARTESIAN_POINT ( 'NONE',  ( 0.000000000000000000, 0.06698729810653621108, 0.000000000000000000 ) ) ;
#189177=AXIS2_PLACEMENT_3D ( 'NONE', #166829, #203553, #151651 ) ;
#190189=SURFACE_STYLE_USAGE ( .BOTH. , #124230 ) ;
#191136=CIRCLE ( 'NONE', #939, 11.09999999999999964 ) ;
#191276=CIRCLE ( 'NONE', #90969, 11.09999999999999964 ) ;
#191412=EDGE_CURVE ( 'NONE', #1071, #103667, #205886, .T. ) ;
#191441=ORIENTED_EDGE ( 'NONE', *, *, #37586, .F. ) ;
#191853=CIRCLE ( 'NONE', #202190, 0.2000000000000005107 ) ;
#192139=( GEOMETRIC_REPRESENTATION_CONTEXT ( 3 ) GLOBAL_UNCERTAINTY_ASSIGNED_CONTEXT ( ( #34464 ) ) GLOBAL_UNIT_ASSIGNED_CONTEXT ( ( #22875, #133496, #142025 ) ) REPRESENTATION_CONTEXT ( 'NONE', 'WORKASPACE' ) );
#192173=DIRECTION ( 'NONE',  ( 1.224646799147343593E-16, 0.000000000000000000, -1.000000000000000000 ) ) ;
#192854=CARTESIAN_POINT ( 'NONE',  ( 0.000000000000000000, 0.5000000000000000000, 0.000000000000000000 ) ) ;
#193470=EDGE_CURVE ( 'NONE', #179011, #1071, #67774, .T. ) ;
#194059=SURFACE_STYLE_USAGE ( .BOTH. , #27292 ) ;
#194643=EDGE_LOOP ( 'NONE', ( #119306, #104995, #37903, #76111 ) ) ;
#194783=TOROIDAL_SURFACE ( 'NONE', #177482, 10.75000000000000000, 0.5000000000000007772 ) ;
#195145=( NAMED_UNIT ( * ) PLANE_ANGLE_UNIT ( ) SI_UNIT ( $, .RADIAN. ) );
#195276=CIRCLE ( 'NONE', #185363, 11.09999999999999964 ) ;
#195576=AXIS2_PLACEMENT_3D ( 'NONE', #56475, #8780, #172364 ) ;
#195629=FACE_OUTER_BOUND ( 'NONE', #175201, .T. ) ;
#196832=AXIS2_PLACEMENT_3D ( 'NONE', #188337, #39976, #172107 ) ;
#196864=PRESENTATION_STYLE_ASSIGNMENT (( #132969 ) ) ;
#197373=ADVANCED_FACE ( 'NONE', ( #134358 ), #154841, .T. ) ;
#197903=SURFACE_SIDE_STYLE ('',( #149166 ) ) ;
#199556=AXIS2_PLACEMENT_3D ( 'NONE', #50616, #116741, #66826 ) ;
#199687=LINE ( 'NONE', #150974, #161195 ) ;
#199834=ORIENTED_EDGE ( 'NONE', *, *, #174601, .T. ) ;
#200407=AXIS2_PLACEMENT_3D ( 'NONE', #95216, #132002, #161266 ) ;
#201227=ORIENTED_EDGE ( 'NONE', *, *, #191412, .F. ) ;
#201573=DIRECTION ( 'NONE',  ( 0.000000000000000000, 1.000000000000000000, 0.000000000000000000 ) ) ;
#202190=AXIS2_PLACEMENT_3D ( 'NONE', #34505, #165579, #17173 ) ;
#202953=COLOUR_RGB ( '', 0.08235294, 0.09019608, 0.10196078) ;
#203462=EDGE_LOOP ( 'NONE', ( #27303, #191441, #158327, #131258, #1194 ) ) ;
#203553=DIRECTION ( 'NONE',  ( 0.000000000000000000, 1.000000000000000000, 0.000000000000000000 ) ) ;
#204374=DIRECTION ( 'NONE',  ( -0.000000000000000000, 1.000000000000000000, -0.000000000000000000 ) ) ;
#204448=DIRECTION ( 'NONE',  ( 1.224646799147353454E-16, 0.000000000000000000, -1.000000000000000000 ) ) ;
#204669=CARTESIAN_POINT ( 'NONE',  ( 10.12374542407608935, 0.7598076211376182387, -4.551898349974264235 ) ) ;
#205256=CIRCLE ( 'NONE', #111974, 10.99999999999718980 ) ;
#205759=FILL_AREA_STYLE ('',( #55261 ) ) ;
#205856=CARTESIAN_POINT ( 'NONE',  ( 0.000000000000000000, 0.9330127018934565308, 0.000000000000000000 ) ) ;
#205886=CIRCLE ( 'NONE', #60703, 10.24999999999999822 ) ;
#206018=EDGE_LOOP ( 'NONE', ( #131518, #124612, #61506, #114626, #124147 ) ) ;
#206105=CARTESIAN_POINT ( 'NONE',  ( -10.12374542407608402, 0.2401923788623722134, 4.551898349974277558 ) ) ;
#206357=ORIENTED_EDGE ( 'NONE', *, *, #174601, .F. ) ;
#206748=DIRECTION ( 'NONE',  ( 0.000000000000000000, 1.000000000000000000, 0.000000000000000000 ) ) ;
#208814=AXIS2_PLACEMENT_3D ( 'NONE', #205856, #201573, #53219 ) ;
#208851=CARTESIAN_POINT ( 'NONE',  ( 3.069588487047325309E-15, 0.7598076211376200151, 10.89999999999921343 ) ) ;
#209008=CARTESIAN_POINT ( 'NONE',  ( 0.000000000000000000, 0.5000000000000000000, 0.000000000000000000 ) ) ;
#209450=MECHANICAL_DESIGN_GEOMETRIC_PRESENTATION_REPRESENTATION('',(#29523),#192139);
#209917=DIRECTION ( 'NONE',  ( -1.224646799147343593E-16, 0.000000000000000000, -1.000000000000000000 ) ) ;
#210305=FILL_AREA_STYLE ('',( #94465 ) ) ;
#210619=CARTESIAN_POINT ( 'NONE',  ( 1.347111479061784496E-15, 0.06698729810653621108, -10.99999999999751665 ) ) ;
#211384=UNCERTAINTY_MEASURE_WITH_UNIT (LENGTH_MEASURE( 1.000000000000000082E-05 ), #123553, 'distance_accuracy_value', 'NONE');
#211736=DIRECTION ( 'NONE',  ( 0.000000000000000000, 0.000000000000000000, 1.000000000000000000 ) ) ;
#212325=CARTESIAN_POINT ( 'NONE',  ( 0.000000000000000000, 0.9330127018934565308, 10.99999999999752553 ) ) ;
#212363=COLOUR_RGB ( '', 0.31764706, 0.68627451, 0.89019608) ;
#212877=PRODUCT_DEFINITION_CONTEXT ( 'detailed design', #110207, 'design' ) ;
ENDSEC;
END-ISO-10303-21;
